ISO-10303-21;
HEADER;
/* Generated by software containing ST-Developer
 * from STEP Tools, Inc. (www.steptools.com) 
 */

FILE_DESCRIPTION(
/* description */ ('PAT-091'),
/* implementation_level */ '2;1');

FILE_NAME(
/* name */ 'M4 low-profile retaining screw (1).step',
/* time_stamp */ '2026-10-27T15:34:44-07:00',
/* author */ (''),
/* organization */ (''),
/* preprocessor_version */ 'ST-DEVELOPER v20.2',
/* originating_system */ 'Autodesk Translation Framework v15.17.0.0',
/* authorisation */ '');

FILE_SCHEMA (('AUTOMOTIVE_DESIGN { 1 0 10303 214 3 1 1 }'));
ENDSEC;

DATA;
#10=MECHANICAL_DESIGN_GEOMETRIC_PRESENTATION_REPRESENTATION('',(#1049),#25100);
#829=SHAPE_REPRESENTATION_RELATIONSHIP('SRR','None',#25596,#939);
#939=ADVANCED_BREP_SHAPE_REPRESENTATION('',(#1170),#25066);
#1049=STYLED_ITEM('',(#26198),#1170);
#1170=MANIFOLD_SOLID_BREP('Body1',#13329);
#1554=FACE_BOUND('',#3809,.T.);
#1963=PLANE('',#15862);
#1964=PLANE('',#15867);
#1965=PLANE('',#15870);
#2651=FACE_OUTER_BOUND('',#3808,.T.);
#2652=FACE_OUTER_BOUND('',#3810,.T.);
#2653=FACE_OUTER_BOUND('',#3811,.T.);
#2654=FACE_OUTER_BOUND('',#3812,.T.);
#2655=FACE_OUTER_BOUND('',#3813,.T.);
#3808=EDGE_LOOP('',(#11306));
#3809=EDGE_LOOP('',(#11307));
#3810=EDGE_LOOP('',(#11308,#11309,#11310,#11311));
#3811=EDGE_LOOP('',(#11312));
#3812=EDGE_LOOP('',(#11313,#11314,#11315,#11316));
#3813=EDGE_LOOP('',(#11317));
#4759=LINE('',#23723,#5499);
#4760=LINE('',#23729,#5500);
#5499=VECTOR('',#19665,0.350000000000001);
#5500=VECTOR('',#19674,0.199999999999999);
#6132=CIRCLE('',#15863,0.350000000000001);
#6133=CIRCLE('',#15864,0.199999999999999);
#6134=CIRCLE('',#15866,0.350000000000001);
#6135=CIRCLE('',#15869,0.199999999999999);
#7157=VERTEX_POINT('',#23717);
#7158=VERTEX_POINT('',#23719);
#7159=VERTEX_POINT('',#23722);
#7160=VERTEX_POINT('',#23727);
#8588=EDGE_CURVE('',#7157,#7157,#6132,.T.);
#8589=EDGE_CURVE('',#7158,#7158,#6133,.T.);
#8590=EDGE_CURVE('',#7157,#7159,#4759,.T.);
#8591=EDGE_CURVE('',#7159,#7159,#6134,.T.);
#8592=EDGE_CURVE('',#7160,#7160,#6135,.T.);
#8593=EDGE_CURVE('',#7160,#7158,#4760,.T.);
#11306=ORIENTED_EDGE('',*,*,#8588,.T.);
#11307=ORIENTED_EDGE('',*,*,#8589,.F.);
#11308=ORIENTED_EDGE('',*,*,#8588,.F.);
#11309=ORIENTED_EDGE('',*,*,#8590,.T.);
#11310=ORIENTED_EDGE('',*,*,#8591,.T.);
#11311=ORIENTED_EDGE('',*,*,#8590,.F.);
#11312=ORIENTED_EDGE('',*,*,#8591,.F.);
#11313=ORIENTED_EDGE('',*,*,#8592,.F.);
#11314=ORIENTED_EDGE('',*,*,#8593,.T.);
#11315=ORIENTED_EDGE('',*,*,#8589,.T.);
#11316=ORIENTED_EDGE('',*,*,#8593,.F.);
#11317=ORIENTED_EDGE('',*,*,#8592,.T.);
#12327=CYLINDRICAL_SURFACE('',#15865,0.350000000000001);
#12328=CYLINDRICAL_SURFACE('',#15868,0.199999999999999);
#13018=ADVANCED_FACE('',(#2651,#1554),#1963,.T.);
#13019=ADVANCED_FACE('',(#2652),#12327,.T.);
#13020=ADVANCED_FACE('',(#2653),#1964,.F.);
#13021=ADVANCED_FACE('',(#2654),#12328,.T.);
#13022=ADVANCED_FACE('',(#2655),#1965,.T.);
#13329=CLOSED_SHELL('',(#13018,#13019,#13020,#13021,#13022));
#15861=AXIS2_PLACEMENT_3D('',#23715,#19655,#19656);
#15862=AXIS2_PLACEMENT_3D('',#23716,#19657,#19658);
#15863=AXIS2_PLACEMENT_3D('',#23718,#19659,#19660);
#15864=AXIS2_PLACEMENT_3D('',#23720,#19661,#19662);
#15865=AXIS2_PLACEMENT_3D('',#23721,#19663,#19664);
#15866=AXIS2_PLACEMENT_3D('',#23724,#19666,#19667);
#15867=AXIS2_PLACEMENT_3D('',#23725,#19668,#19669);
#15868=AXIS2_PLACEMENT_3D('',#23726,#19670,#19671);
#15869=AXIS2_PLACEMENT_3D('',#23728,#19672,#19673);
#15870=AXIS2_PLACEMENT_3D('',#23730,#19675,#19676);
#19655=DIRECTION('axis',(0.,0.,1.));
#19656=DIRECTION('refdir',(1.,0.,0.));
#19657=DIRECTION('center_axis',(0.,1.,0.));
#19658=DIRECTION('ref_axis',(1.,0.,0.));
#19659=DIRECTION('center_axis',(0.,1.,0.));
#19660=DIRECTION('ref_axis',(1.,0.,0.));
#19661=DIRECTION('center_axis',(0.,1.,0.));
#19662=DIRECTION('ref_axis',(1.,0.,0.));
#19663=DIRECTION('center_axis',(0.,1.,0.));
#19664=DIRECTION('ref_axis',(1.,0.,0.));
#19665=DIRECTION('',(0.,-1.,0.));
#19666=DIRECTION('center_axis',(0.,1.,0.));
#19667=DIRECTION('ref_axis',(1.,0.,0.));
#19668=DIRECTION('center_axis',(0.,1.,0.));
#19669=DIRECTION('ref_axis',(1.,0.,0.));
#19670=DIRECTION('center_axis',(0.,1.,0.));
#19671=DIRECTION('ref_axis',(1.,0.,0.));
#19672=DIRECTION('center_axis',(0.,1.,0.));
#19673=DIRECTION('ref_axis',(1.,0.,0.));
#19674=DIRECTION('',(0.,-1.,0.));
#19675=DIRECTION('center_axis',(0.,1.,0.));
#19676=DIRECTION('ref_axis',(1.,0.,0.));
#23715=CARTESIAN_POINT('',(0.,0.,0.));
#23716=CARTESIAN_POINT('Origin',(18.056769185842,-5.8,9.30814754519511));
#23717=CARTESIAN_POINT('',(17.706769185842,-5.8,9.30814754519511));
#23718=CARTESIAN_POINT('Origin',(18.056769185842,-5.8,9.30814754519511));
#23719=CARTESIAN_POINT('',(17.856769185842,-5.8,9.30814754519511));
#23720=CARTESIAN_POINT('Origin',(18.056769185842,-5.8,9.30814754519511));
#23721=CARTESIAN_POINT('Origin',(18.056769185842,-5.9,9.30814754519511));
#23722=CARTESIAN_POINT('',(17.706769185842,-5.9,9.30814754519511));
#23723=CARTESIAN_POINT('',(17.706769185842,-5.9,9.30814754519511));
#23724=CARTESIAN_POINT('Origin',(18.056769185842,-5.9,9.30814754519511));
#23725=CARTESIAN_POINT('Origin',(18.056769185842,-5.9,9.30814754519511));
#23726=CARTESIAN_POINT('Origin',(18.056769185842,-5.8,9.30814754519511));
#23727=CARTESIAN_POINT('',(17.856769185842,-5.1,9.30814754519511));
#23728=CARTESIAN_POINT('Origin',(18.056769185842,-5.1,9.30814754519511));
#23729=CARTESIAN_POINT('',(17.856769185842,-5.8,9.30814754519511));
#23730=CARTESIAN_POINT('Origin',(18.056769185842,-5.1,9.30814754519511));
#24945=UNCERTAINTY_MEASURE_WITH_UNIT(LENGTH_MEASURE(0.001),#25101,
'DISTANCE_ACCURACY_VALUE',
'Maximum model space distance between geometric entities at asserted c
onnectivities');
#24979=UNCERTAINTY_MEASURE_WITH_UNIT(LENGTH_MEASURE(0.001),#25101,
'DISTANCE_ACCURACY_VALUE',
'Maximum model space distance between geometric entities at asserted c
onnectivities');
#25066=(
GEOMETRIC_REPRESENTATION_CONTEXT(3)
GLOBAL_UNCERTAINTY_ASSIGNED_CONTEXT((#24945))
GLOBAL_UNIT_ASSIGNED_CONTEXT((#25101,#25103,#25104))
REPRESENTATION_CONTEXT('','3D')
);
#25100=(
GEOMETRIC_REPRESENTATION_CONTEXT(3)
GLOBAL_UNCERTAINTY_ASSIGNED_CONTEXT((#24979))
GLOBAL_UNIT_ASSIGNED_CONTEXT((#25101,#25103,#25104))
REPRESENTATION_CONTEXT('','3D')
);
#25101=(
LENGTH_UNIT()
NAMED_UNIT(*)
SI_UNIT(.CENTI.,.METRE.)
);
#25103=(
NAMED_UNIT(*)
PLANE_ANGLE_UNIT()
SI_UNIT($,.RADIAN.)
);
#25104=(
NAMED_UNIT(*)
SI_UNIT($,.STERADIAN.)
SOLID_ANGLE_UNIT()
);
#25191=SHAPE_DEFINITION_REPRESENTATION(#25385,#25596);
#25385=PRODUCT_DEFINITION_SHAPE('',$,#25717);
#25596=SHAPE_REPRESENTATION('',(#15861),#25066);
#25630=PRODUCT_DEFINITION_CONTEXT('part definition',#25992,'design');
#25717=PRODUCT_DEFINITION('M4 low-profile retaining screw (1)',
'M4 low-profile retaining screw (1)',#25837,#25630);
#25837=PRODUCT_DEFINITION_FORMATION('',$,#26080);
#25992=APPLICATION_CONTEXT(
'Core Data for Automotive Mechanical Design Process');
#25993=PRODUCT_CONTEXT('part definition',#25992,'mechanical');
#26080=PRODUCT('M4 low-profile retaining screw (1)',
'M4 low-profile retaining screw (1)','M4 low-profile retaining screw (1)',(#25993));
#26192=COLOUR_RGB('Black',0.12,0.14,0.17);
#26193=FILL_AREA_STYLE_COLOUR('',#26192);
#26194=FILL_AREA_STYLE('',(#26193));
#26195=SURFACE_STYLE_FILL_AREA(#26194);
#26196=SURFACE_SIDE_STYLE('',(#26195));
#26197=SURFACE_STYLE_USAGE(.BOTH.,#26196);
#26198=PRESENTATION_STYLE_ASSIGNMENT((#26197));
ENDSEC;
END-ISO-10303-21;
